ISO-10303-21;
HEADER;
/* Generated by software containing ST-Developer
 * from STEP Tools, Inc. (www.steptools.com) 
 */

FILE_DESCRIPTION(
/* description */ ('Shaft runout checking stand'),
/* implementation_level */ '2;1');

FILE_NAME(
/* name */ 'Dead axle (1).step',
/* time_stamp */ '2026-11-02T21:12:33-08:00',
/* author */ (''),
/* organization */ (''),
/* preprocessor_version */ 'ST-DEVELOPER v20.2',
/* originating_system */ 'Autodesk Translation Framework v15.17.0.0',
/* authorisation */ '');

FILE_SCHEMA (('AUTOMOTIVE_DESIGN { 1 0 10303 214 3 1 1 }'));
ENDSEC;

DATA;
#10=MECHANICAL_DESIGN_GEOMETRIC_PRESENTATION_REPRESENTATION('',(#474),#11748);
#388=SHAPE_REPRESENTATION_RELATIONSHIP('SRR','None',#11937,#431);
#431=ADVANCED_BREP_SHAPE_REPRESENTATION('',(#525),#11713);
#474=STYLED_ITEM('',(#12169),#525);
#525=MANIFOLD_SOLID_BREP('Body1',#6217);
#607=FACE_BOUND('',#1583,.T.);
#608=FACE_BOUND('',#1588,.T.);
#736=CIRCLE('',#6943,0.165);
#737=CIRCLE('',#6944,0.165);
#738=CIRCLE('',#6947,0.8);
#739=CIRCLE('',#6948,0.5);
#740=CIRCLE('',#6950,0.8);
#741=CIRCLE('',#6953,0.5);
#968=CYLINDRICAL_SURFACE('',#6942,0.165);
#969=CYLINDRICAL_SURFACE('',#6949,0.8);
#970=CYLINDRICAL_SURFACE('',#6952,0.5);
#1167=FACE_OUTER_BOUND('',#1580,.T.);
#1168=FACE_OUTER_BOUND('',#1581,.T.);
#1169=FACE_OUTER_BOUND('',#1582,.T.);
#1170=FACE_OUTER_BOUND('',#1584,.T.);
#1171=FACE_OUTER_BOUND('',#1585,.T.);
#1172=FACE_OUTER_BOUND('',#1586,.T.);
#1173=FACE_OUTER_BOUND('',#1587,.T.);
#1580=EDGE_LOOP('',(#4722,#4723,#4724,#4725));
#1581=EDGE_LOOP('',(#4726));
#1582=EDGE_LOOP('',(#4727));
#1583=EDGE_LOOP('',(#4728));
#1584=EDGE_LOOP('',(#4729,#4730,#4731,#4732));
#1585=EDGE_LOOP('',(#4733));
#1586=EDGE_LOOP('',(#4734,#4735,#4736,#4737));
#1587=EDGE_LOOP('',(#4738));
#1588=EDGE_LOOP('',(#4739));
#2137=LINE('',#10150,#2604);
#2138=LINE('',#10160,#2605);
#2139=LINE('',#10166,#2606);
#2604=VECTOR('',#8164,0.165);
#2605=VECTOR('',#8177,0.8);
#2606=VECTOR('',#8186,0.5);
#3030=VERTEX_POINT('',#10147);
#3031=VERTEX_POINT('',#10149);
#3032=VERTEX_POINT('',#10154);
#3033=VERTEX_POINT('',#10156);
#3034=VERTEX_POINT('',#10159);
#3035=VERTEX_POINT('',#10164);
#3647=EDGE_CURVE('',#3030,#3030,#736,.T.);
#3648=EDGE_CURVE('',#3030,#3031,#2137,.T.);
#3649=EDGE_CURVE('',#3031,#3031,#737,.T.);
#3650=EDGE_CURVE('',#3032,#3032,#738,.T.);
#3651=EDGE_CURVE('',#3033,#3033,#739,.T.);
#3652=EDGE_CURVE('',#3032,#3034,#2138,.T.);
#3653=EDGE_CURVE('',#3034,#3034,#740,.T.);
#3654=EDGE_CURVE('',#3035,#3035,#741,.T.);
#3655=EDGE_CURVE('',#3035,#3033,#2139,.T.);
#4722=ORIENTED_EDGE('',*,*,#3647,.F.);
#4723=ORIENTED_EDGE('',*,*,#3648,.T.);
#4724=ORIENTED_EDGE('',*,*,#3649,.F.);
#4725=ORIENTED_EDGE('',*,*,#3648,.F.);
#4726=ORIENTED_EDGE('',*,*,#3647,.T.);
#4727=ORIENTED_EDGE('',*,*,#3650,.T.);
#4728=ORIENTED_EDGE('',*,*,#3651,.F.);
#4729=ORIENTED_EDGE('',*,*,#3650,.F.);
#4730=ORIENTED_EDGE('',*,*,#3652,.T.);
#4731=ORIENTED_EDGE('',*,*,#3653,.T.);
#4732=ORIENTED_EDGE('',*,*,#3652,.F.);
#4733=ORIENTED_EDGE('',*,*,#3653,.F.);
#4734=ORIENTED_EDGE('',*,*,#3654,.F.);
#4735=ORIENTED_EDGE('',*,*,#3655,.T.);
#4736=ORIENTED_EDGE('',*,*,#3651,.T.);
#4737=ORIENTED_EDGE('',*,*,#3655,.F.);
#4738=ORIENTED_EDGE('',*,*,#3654,.T.);
#4739=ORIENTED_EDGE('',*,*,#3649,.T.);
#5702=PLANE('',#6945);
#5703=PLANE('',#6946);
#5704=PLANE('',#6951);
#5705=PLANE('',#6954);
#5967=ADVANCED_FACE('',(#1167),#968,.F.);
#5968=ADVANCED_FACE('',(#1168),#5702,.T.);
#5969=ADVANCED_FACE('',(#1169,#607),#5703,.T.);
#5970=ADVANCED_FACE('',(#1170),#969,.T.);
#5971=ADVANCED_FACE('',(#1171),#5704,.F.);
#5972=ADVANCED_FACE('',(#1172),#970,.T.);
#5973=ADVANCED_FACE('',(#1173,#608),#5705,.T.);
#6217=CLOSED_SHELL('',(#5967,#5968,#5969,#5970,#5971,#5972,#5973));
#6941=AXIS2_PLACEMENT_3D('',#10145,#8158,#8159);
#6942=AXIS2_PLACEMENT_3D('',#10146,#8160,#8161);
#6943=AXIS2_PLACEMENT_3D('',#10148,#8162,#8163);
#6944=AXIS2_PLACEMENT_3D('',#10151,#8165,#8166);
#6945=AXIS2_PLACEMENT_3D('',#10152,#8167,#8168);
#6946=AXIS2_PLACEMENT_3D('',#10153,#8169,#8170);
#6947=AXIS2_PLACEMENT_3D('',#10155,#8171,#8172);
#6948=AXIS2_PLACEMENT_3D('',#10157,#8173,#8174);
#6949=AXIS2_PLACEMENT_3D('',#10158,#8175,#8176);
#6950=AXIS2_PLACEMENT_3D('',#10161,#8178,#8179);
#6951=AXIS2_PLACEMENT_3D('',#10162,#8180,#8181);
#6952=AXIS2_PLACEMENT_3D('',#10163,#8182,#8183);
#6953=AXIS2_PLACEMENT_3D('',#10165,#8184,#8185);
#6954=AXIS2_PLACEMENT_3D('',#10167,#8187,#8188);
#8158=DIRECTION('axis',(0.,0.,1.));
#8159=DIRECTION('refdir',(1.,0.,0.));
#8160=DIRECTION('center_axis',(0.,1.,0.));
#8161=DIRECTION('ref_axis',(1.,0.,0.));
#8162=DIRECTION('center_axis',(0.,1.,0.));
#8163=DIRECTION('ref_axis',(1.,0.,0.));
#8164=DIRECTION('',(0.,1.,0.));
#8165=DIRECTION('center_axis',(0.,-1.,0.));
#8166=DIRECTION('ref_axis',(1.,0.,0.));
#8167=DIRECTION('center_axis',(0.,1.,0.));
#8168=DIRECTION('ref_axis',(1.,0.,0.));
#8169=DIRECTION('center_axis',(0.,1.,0.));
#8170=DIRECTION('ref_axis',(1.,0.,0.));
#8171=DIRECTION('center_axis',(0.,1.,0.));
#8172=DIRECTION('ref_axis',(1.,0.,0.));
#8173=DIRECTION('center_axis',(0.,1.,0.));
#8174=DIRECTION('ref_axis',(1.,0.,0.));
#8175=DIRECTION('center_axis',(0.,1.,0.));
#8176=DIRECTION('ref_axis',(1.,0.,0.));
#8177=DIRECTION('',(0.,-1.,0.));
#8178=DIRECTION('center_axis',(0.,1.,0.));
#8179=DIRECTION('ref_axis',(1.,0.,0.));
#8180=DIRECTION('center_axis',(0.,1.,0.));
#8181=DIRECTION('ref_axis',(1.,0.,0.));
#8182=DIRECTION('center_axis',(0.,1.,0.));
#8183=DIRECTION('ref_axis',(1.,0.,0.));
#8184=DIRECTION('center_axis',(0.,1.,0.));
#8185=DIRECTION('ref_axis',(1.,0.,0.));
#8186=DIRECTION('',(0.,-1.,0.));
#8187=DIRECTION('center_axis',(0.,1.,0.));
#8188=DIRECTION('ref_axis',(1.,0.,0.));
#10145=CARTESIAN_POINT('',(0.,0.,0.));
#10146=CARTESIAN_POINT('Origin',(2.,-10.4,5.));
#10147=CARTESIAN_POINT('',(1.835,-10.4,5.));
#10148=CARTESIAN_POINT('Origin',(2.,-10.4,5.));
#10149=CARTESIAN_POINT('',(1.835,-9.2,5.));
#10150=CARTESIAN_POINT('',(1.835,-10.4,5.));
#10151=CARTESIAN_POINT('Origin',(2.,-9.2,5.));
#10152=CARTESIAN_POINT('Origin',(2.,-10.4,5.));
#10153=CARTESIAN_POINT('Origin',(2.,-11.5,5.));
#10154=CARTESIAN_POINT('',(1.2,-11.5,5.));
#10155=CARTESIAN_POINT('Origin',(2.,-11.5,5.));
#10156=CARTESIAN_POINT('',(1.5,-11.5,5.));
#10157=CARTESIAN_POINT('Origin',(2.,-11.5,5.));
#10158=CARTESIAN_POINT('Origin',(2.,-11.8,5.));
#10159=CARTESIAN_POINT('',(1.2,-11.8,5.));
#10160=CARTESIAN_POINT('',(1.2,-11.8,5.));
#10161=CARTESIAN_POINT('Origin',(2.,-11.8,5.));
#10162=CARTESIAN_POINT('Origin',(2.,-11.8,5.));
#10163=CARTESIAN_POINT('Origin',(2.,-11.5,5.));
#10164=CARTESIAN_POINT('',(1.5,-9.2,5.));
#10165=CARTESIAN_POINT('Origin',(2.,-9.2,5.));
#10166=CARTESIAN_POINT('',(1.5,-11.5,5.));
#10167=CARTESIAN_POINT('Origin',(2.,-9.2,5.));
#11664=UNCERTAINTY_MEASURE_WITH_UNIT(LENGTH_MEASURE(0.001),#11749,
'DISTANCE_ACCURACY_VALUE',
'Maximum model space distance between geometric entities at asserted c
onnectivities');
#11699=UNCERTAINTY_MEASURE_WITH_UNIT(LENGTH_MEASURE(0.001),#11749,
'DISTANCE_ACCURACY_VALUE',
'Maximum model space distance between geometric entities at asserted c
onnectivities');
#11713=(
GEOMETRIC_REPRESENTATION_CONTEXT(3)
GLOBAL_UNCERTAINTY_ASSIGNED_CONTEXT((#11664))
GLOBAL_UNIT_ASSIGNED_CONTEXT((#11749,#11751,#11752))
REPRESENTATION_CONTEXT('','3D')
);
#11748=(
GEOMETRIC_REPRESENTATION_CONTEXT(3)
GLOBAL_UNCERTAINTY_ASSIGNED_CONTEXT((#11699))
GLOBAL_UNIT_ASSIGNED_CONTEXT((#11749,#11751,#11752))
REPRESENTATION_CONTEXT('','3D')
);
#11749=(
LENGTH_UNIT()
NAMED_UNIT(*)
SI_UNIT(.CENTI.,.METRE.)
);
#11751=(
NAMED_UNIT(*)
PLANE_ANGLE_UNIT()
SI_UNIT($,.RADIAN.)
);
#11752=(
NAMED_UNIT(*)
SI_UNIT($,.STERADIAN.)
SOLID_ANGLE_UNIT()
);
#11766=SHAPE_DEFINITION_REPRESENTATION(#11814,#11937);
#11814=PRODUCT_DEFINITION_SHAPE('',$,#11986);
#11937=SHAPE_REPRESENTATION('',(#6941),#11713);
#11972=PRODUCT_DEFINITION_CONTEXT('part definition',#12118,'design');
#11986=PRODUCT_DEFINITION('Dead axle_1','Dead axle (1)',#12034,#11972);
#12034=PRODUCT_DEFINITION_FORMATION('',$,#12133);
#12118=APPLICATION_CONTEXT(
'Core Data for Automotive Mechanical Design Process');
#12119=PRODUCT_CONTEXT('part definition',#12118,'mechanical');
#12133=PRODUCT('Dead axle_1','Dead axle (1)','Dead axle',(#12119));
#12169=PRESENTATION_STYLE_ASSIGNMENT((#12174));
#12174=SURFACE_STYLE_USAGE(.BOTH.,#12179);
#12179=SURFACE_SIDE_STYLE('',(#12184));
#12184=SURFACE_STYLE_FILL_AREA(#12189);
#12189=FILL_AREA_STYLE('CAD Library Painted - Engineering blue',(#12194));
#12194=FILL_AREA_STYLE_COLOUR('CAD Library Painted - Engineering blue',
#12199);
#12199=COLOUR_RGB('CAD Library Painted - Engineering blue',0.12156862745098,
0.356862745098039,0.6);
ENDSEC;
END-ISO-10303-21;
